ISO-10303-21;
HEADER;
/* Generated by software containing ST-Developer
 * from STEP Tools, Inc. (www.steptools.com) 
 */

FILE_DESCRIPTION(
/* description */ ('Timing belt drive module 2 mm Pitch Timing 20T-40T'),

/* implementation_level */ '2;1');

FILE_NAME(
/* name */ 'Cap Screw - M4x16.step',
/* time_stamp */ '2026-10-28T03:25:12-07:00',
/* author */ (''),
/* organization */ (''),
/* preprocessor_version */ 'ST-DEVELOPER v20.2',
/* originating_system */ 'Autodesk Translation Framework v15.17.0.0',
/* authorisation */ '');

FILE_SCHEMA (('AUTOMOTIVE_DESIGN { 1 0 10303 214 3 1 1 }'));
ENDSEC;

DATA;
#10=MECHANICAL_DESIGN_GEOMETRIC_PRESENTATION_REPRESENTATION('',(#581),#17830);
#13=ORIENTED_CLOSED_SHELL('',*,#9041,.F.);
#16=BREP_WITH_VOIDS('Body1',#9040,(#13));
#430=CONICAL_SURFACE('',#10723,0.325,0.785398163397448);
#431=CONICAL_SURFACE('',#10727,0.335,0.785398163397448);
#432=CONICAL_SURFACE('',#10731,0.21,0.463647609000806);
#433=CONICAL_SURFACE('',#10735,0.18,0.785398163397448);
#480=SHAPE_REPRESENTATION_RELATIONSHIP('SRR','None',#18054,#523);
#523=ADVANCED_BREP_SHAPE_REPRESENTATION('',(#16),#17829);
#581=STYLED_ITEM('',(#18324),#16);
#772=FACE_BOUND('',#2127,.T.);
#951=PLANE('',#10721);
#952=PLANE('',#10729);
#953=PLANE('',#10737);
#954=PLANE('',#10738);
#955=PLANE('',#10739);
#956=PLANE('',#10740);
#957=PLANE('',#10741);
#958=PLANE('',#10742);
#959=PLANE('',#10743);
#960=PLANE('',#10744);
#961=PLANE('',#10745);
#1466=FACE_OUTER_BOUND('',#2122,.T.);
#1467=FACE_OUTER_BOUND('',#2123,.T.);
#1468=FACE_OUTER_BOUND('',#2124,.T.);
#1469=FACE_OUTER_BOUND('',#2125,.T.);
#1470=FACE_OUTER_BOUND('',#2126,.T.);
#1471=FACE_OUTER_BOUND('',#2128,.T.);
#1472=FACE_OUTER_BOUND('',#2129,.T.);
#1473=FACE_OUTER_BOUND('',#2130,.T.);
#1474=FACE_OUTER_BOUND('',#2131,.T.);
#1475=FACE_OUTER_BOUND('',#2132,.T.);
#1476=FACE_OUTER_BOUND('',#2133,.T.);
#1477=FACE_OUTER_BOUND('',#2134,.T.);
#1478=FACE_OUTER_BOUND('',#2135,.T.);
#1479=FACE_OUTER_BOUND('',#2136,.T.);
#1480=FACE_OUTER_BOUND('',#2137,.T.);
#1481=FACE_OUTER_BOUND('',#2138,.T.);
#1482=FACE_OUTER_BOUND('',#2139,.T.);
#2122=EDGE_LOOP('',(#8117));
#2123=EDGE_LOOP('',(#8118,#8119,#8120,#8121));
#2124=EDGE_LOOP('',(#8122,#8123,#8124,#8125));
#2125=EDGE_LOOP('',(#8126,#8127,#8128,#8129));
#2126=EDGE_LOOP('',(#8130));
#2127=EDGE_LOOP('',(#8131));
#2128=EDGE_LOOP('',(#8132,#8133,#8134,#8135));
#2129=EDGE_LOOP('',(#8136,#8137,#8138,#8139));
#2130=EDGE_LOOP('',(#8140,#8141,#8142,#8143));
#2131=EDGE_LOOP('',(#8144));
#2132=EDGE_LOOP('',(#8145,#8146,#8147,#8148));
#2133=EDGE_LOOP('',(#8149,#8150,#8151,#8152));
#2134=EDGE_LOOP('',(#8153,#8154,#8155,#8156));
#2135=EDGE_LOOP('',(#8157,#8158,#8159,#8160));
#2136=EDGE_LOOP('',(#8161,#8162,#8163,#8164));
#2137=EDGE_LOOP('',(#8165,#8166,#8167,#8168));
#2138=EDGE_LOOP('',(#8169,#8170,#8171,#8172,#8173,#8174));
#2139=EDGE_LOOP('',(#8175,#8176,#8177,#8178,#8179,#8180));
#2782=CIRCLE('',#10722,0.3);
#2783=CIRCLE('',#10724,0.35);
#2784=CIRCLE('',#10726,0.35);
#2785=CIRCLE('',#10728,0.32);
#2786=CIRCLE('',#10730,0.22);
#2787=CIRCLE('',#10732,0.1954);
#2788=CIRCLE('',#10734,0.1954);
#2789=CIRCLE('',#10736,0.16);
#3244=LINE('',#17605,#3722);
#3245=LINE('',#17609,#3723);
#3246=LINE('',#17613,#3724);
#3247=LINE('',#17620,#3725);
#3248=LINE('',#17624,#3726);
#3249=LINE('',#17628,#3727);
#3250=LINE('',#17633,#3728);
#3251=LINE('',#17635,#3729);
#3252=LINE('',#17637,#3730);
#3253=LINE('',#17638,#3731);
#3254=LINE('',#17641,#3732);
#3255=LINE('',#17643,#3733);
#3256=LINE('',#17644,#3734);
#3257=LINE('',#17647,#3735);
#3258=LINE('',#17649,#3736);
#3259=LINE('',#17650,#3737);
#3260=LINE('',#17653,#3738);
#3261=LINE('',#17655,#3739);
#3262=LINE('',#17656,#3740);
#3263=LINE('',#17659,#3741);
#3264=LINE('',#17661,#3742);
#3265=LINE('',#17662,#3743);
#3266=LINE('',#17664,#3744);
#3267=LINE('',#17665,#3745);
#3722=VECTOR('',#13681,0.325);
#3723=VECTOR('',#13686,0.35);
#3724=VECTOR('',#13691,0.335);
#3725=VECTOR('',#13700,0.21);
#3726=VECTOR('',#13705,0.2);
#3727=VECTOR('',#13710,0.18);
#3728=VECTOR('',#13715,1.);
#3729=VECTOR('',#13716,1.);
#3730=VECTOR('',#13717,1.);
#3731=VECTOR('',#13718,1.);
#3732=VECTOR('',#13721,1.);
#3733=VECTOR('',#13722,1.);
#3734=VECTOR('',#13723,1.);
#3735=VECTOR('',#13726,1.);
#3736=VECTOR('',#13727,1.);
#3737=VECTOR('',#13728,1.);
#3738=VECTOR('',#13731,1.);
#3739=VECTOR('',#13732,1.);
#3740=VECTOR('',#13733,1.);
#3741=VECTOR('',#13736,1.);
#3742=VECTOR('',#13737,1.);
#3743=VECTOR('',#13738,1.);
#3744=VECTOR('',#13741,1.);
#3745=VECTOR('',#13742,1.);
#4549=VERTEX_POINT('',#17600);
#4550=VERTEX_POINT('',#17603);
#4551=VERTEX_POINT('',#17607);
#4552=VERTEX_POINT('',#17611);
#4553=VERTEX_POINT('',#17615);
#4554=VERTEX_POINT('',#17618);
#4555=VERTEX_POINT('',#17622);
#4556=VERTEX_POINT('',#17626);
#4557=VERTEX_POINT('',#17631);
#4558=VERTEX_POINT('',#17632);
#4559=VERTEX_POINT('',#17634);
#4560=VERTEX_POINT('',#17636);
#4561=VERTEX_POINT('',#17640);
#4562=VERTEX_POINT('',#17642);
#4563=VERTEX_POINT('',#17646);
#4564=VERTEX_POINT('',#17648);
#4565=VERTEX_POINT('',#17652);
#4566=VERTEX_POINT('',#17654);
#4567=VERTEX_POINT('',#17658);
#4568=VERTEX_POINT('',#17660);
#5741=EDGE_CURVE('',#4549,#4549,#2782,.T.);
#5742=EDGE_CURVE('',#4550,#4550,#2783,.T.);
#5743=EDGE_CURVE('',#4550,#4549,#3244,.T.);
#5744=EDGE_CURVE('',#4551,#4551,#2784,.T.);
#5745=EDGE_CURVE('',#4551,#4550,#3245,.T.);
#5746=EDGE_CURVE('',#4552,#4552,#2785,.T.);
#5747=EDGE_CURVE('',#4552,#4551,#3246,.T.);
#5748=EDGE_CURVE('',#4553,#4553,#2786,.T.);
#5749=EDGE_CURVE('',#4554,#4554,#2787,.F.);
#5750=EDGE_CURVE('',#4554,#4553,#3247,.T.);
#5751=EDGE_CURVE('',#4555,#4555,#2788,.F.);
#5752=EDGE_CURVE('',#4555,#4554,#3248,.T.);
#5753=EDGE_CURVE('',#4556,#4556,#2789,.T.);
#5754=EDGE_CURVE('',#4556,#4555,#3249,.T.);
#5755=EDGE_CURVE('',#4557,#4558,#3250,.T.);
#5756=EDGE_CURVE('',#4558,#4559,#3251,.T.);
#5757=EDGE_CURVE('',#4559,#4560,#3252,.T.);
#5758=EDGE_CURVE('',#4557,#4560,#3253,.T.);
#5759=EDGE_CURVE('',#4558,#4561,#3254,.T.);
#5760=EDGE_CURVE('',#4561,#4562,#3255,.T.);
#5761=EDGE_CURVE('',#4562,#4559,#3256,.T.);
#5762=EDGE_CURVE('',#4561,#4563,#3257,.T.);
#5763=EDGE_CURVE('',#4563,#4564,#3258,.T.);
#5764=EDGE_CURVE('',#4564,#4562,#3259,.T.);
#5765=EDGE_CURVE('',#4563,#4565,#3260,.T.);
#5766=EDGE_CURVE('',#4565,#4566,#3261,.T.);
#5767=EDGE_CURVE('',#4566,#4564,#3262,.T.);
#5768=EDGE_CURVE('',#4565,#4567,#3263,.T.);
#5769=EDGE_CURVE('',#4567,#4568,#3264,.T.);
#5770=EDGE_CURVE('',#4568,#4566,#3265,.T.);
#5771=EDGE_CURVE('',#4567,#4557,#3266,.T.);
#5772=EDGE_CURVE('',#4560,#4568,#3267,.T.);
#8117=ORIENTED_EDGE('',*,*,#5741,.F.);
#8118=ORIENTED_EDGE('',*,*,#5742,.F.);
#8119=ORIENTED_EDGE('',*,*,#5743,.T.);
#8120=ORIENTED_EDGE('',*,*,#5741,.T.);
#8121=ORIENTED_EDGE('',*,*,#5743,.F.);
#8122=ORIENTED_EDGE('',*,*,#5744,.F.);
#8123=ORIENTED_EDGE('',*,*,#5745,.T.);
#8124=ORIENTED_EDGE('',*,*,#5742,.T.);
#8125=ORIENTED_EDGE('',*,*,#5745,.F.);
#8126=ORIENTED_EDGE('',*,*,#5746,.F.);
#8127=ORIENTED_EDGE('',*,*,#5747,.T.);
#8128=ORIENTED_EDGE('',*,*,#5744,.T.);
#8129=ORIENTED_EDGE('',*,*,#5747,.F.);
#8130=ORIENTED_EDGE('',*,*,#5746,.T.);
#8131=ORIENTED_EDGE('',*,*,#5748,.F.);
#8132=ORIENTED_EDGE('',*,*,#5749,.F.);
#8133=ORIENTED_EDGE('',*,*,#5750,.T.);
#8134=ORIENTED_EDGE('',*,*,#5748,.T.);
#8135=ORIENTED_EDGE('',*,*,#5750,.F.);
#8136=ORIENTED_EDGE('',*,*,#5751,.F.);
#8137=ORIENTED_EDGE('',*,*,#5752,.T.);
#8138=ORIENTED_EDGE('',*,*,#5749,.T.);
#8139=ORIENTED_EDGE('',*,*,#5752,.F.);
#8140=ORIENTED_EDGE('',*,*,#5753,.F.);
#8141=ORIENTED_EDGE('',*,*,#5754,.T.);
#8142=ORIENTED_EDGE('',*,*,#5751,.T.);
#8143=ORIENTED_EDGE('',*,*,#5754,.F.);
#8144=ORIENTED_EDGE('',*,*,#5753,.T.);
#8145=ORIENTED_EDGE('',*,*,#5755,.T.);
#8146=ORIENTED_EDGE('',*,*,#5756,.T.);
#8147=ORIENTED_EDGE('',*,*,#5757,.T.);
#8148=ORIENTED_EDGE('',*,*,#5758,.F.);
#8149=ORIENTED_EDGE('',*,*,#5759,.T.);
#8150=ORIENTED_EDGE('',*,*,#5760,.T.);
#8151=ORIENTED_EDGE('',*,*,#5761,.T.);
#8152=ORIENTED_EDGE('',*,*,#5756,.F.);
#8153=ORIENTED_EDGE('',*,*,#5762,.T.);
#8154=ORIENTED_EDGE('',*,*,#5763,.T.);
#8155=ORIENTED_EDGE('',*,*,#5764,.T.);
#8156=ORIENTED_EDGE('',*,*,#5760,.F.);
#8157=ORIENTED_EDGE('',*,*,#5765,.T.);
#8158=ORIENTED_EDGE('',*,*,#5766,.T.);
#8159=ORIENTED_EDGE('',*,*,#5767,.T.);
#8160=ORIENTED_EDGE('',*,*,#5763,.F.);
#8161=ORIENTED_EDGE('',*,*,#5768,.T.);
#8162=ORIENTED_EDGE('',*,*,#5769,.T.);
#8163=ORIENTED_EDGE('',*,*,#5770,.T.);
#8164=ORIENTED_EDGE('',*,*,#5766,.F.);
#8165=ORIENTED_EDGE('',*,*,#5771,.T.);
#8166=ORIENTED_EDGE('',*,*,#5758,.T.);
#8167=ORIENTED_EDGE('',*,*,#5772,.T.);
#8168=ORIENTED_EDGE('',*,*,#5769,.F.);
#8169=ORIENTED_EDGE('',*,*,#5771,.F.);
#8170=ORIENTED_EDGE('',*,*,#5768,.F.);
#8171=ORIENTED_EDGE('',*,*,#5765,.F.);
#8172=ORIENTED_EDGE('',*,*,#5762,.F.);
#8173=ORIENTED_EDGE('',*,*,#5759,.F.);
#8174=ORIENTED_EDGE('',*,*,#5755,.F.);
#8175=ORIENTED_EDGE('',*,*,#5772,.F.);
#8176=ORIENTED_EDGE('',*,*,#5757,.F.);
#8177=ORIENTED_EDGE('',*,*,#5761,.F.);
#8178=ORIENTED_EDGE('',*,*,#5764,.F.);
#8179=ORIENTED_EDGE('',*,*,#5767,.F.);
#8180=ORIENTED_EDGE('',*,*,#5770,.F.);
#8458=CYLINDRICAL_SURFACE('',#10725,0.35);
#8459=CYLINDRICAL_SURFACE('',#10733,0.1954);
#8964=ADVANCED_FACE('',(#1466),#951,.T.);
#8965=ADVANCED_FACE('',(#1467),#430,.T.);
#8966=ADVANCED_FACE('',(#1468),#8458,.T.);
#8967=ADVANCED_FACE('',(#1469),#431,.T.);
#8968=ADVANCED_FACE('',(#1470,#772),#952,.T.);
#8969=ADVANCED_FACE('',(#1471),#432,.T.);
#8970=ADVANCED_FACE('',(#1472),#8459,.T.);
#8971=ADVANCED_FACE('',(#1473),#433,.T.);
#8972=ADVANCED_FACE('',(#1474),#953,.T.);
#8973=ADVANCED_FACE('',(#1475),#954,.F.);
#8974=ADVANCED_FACE('',(#1476),#955,.F.);
#8975=ADVANCED_FACE('',(#1477),#956,.F.);
#8976=ADVANCED_FACE('',(#1478),#957,.F.);
#8977=ADVANCED_FACE('',(#1479),#958,.F.);
#8978=ADVANCED_FACE('',(#1480),#959,.F.);
#8979=ADVANCED_FACE('',(#1481),#960,.F.);
#8980=ADVANCED_FACE('',(#1482),#961,.F.);
#9040=CLOSED_SHELL('',(#8964,#8965,#8966,#8967,#8968,#8969,#8970,#8971,
#8972));
#9041=CLOSED_SHELL('',(#8973,#8974,#8975,#8976,#8977,#8978,#8979,#8980));
#10720=AXIS2_PLACEMENT_3D('',#17598,#13671,#13672);
#10721=AXIS2_PLACEMENT_3D('',#17599,#13673,#13674);
#10722=AXIS2_PLACEMENT_3D('',#17601,#13675,#13676);
#10723=AXIS2_PLACEMENT_3D('',#17602,#13677,#13678);
#10724=AXIS2_PLACEMENT_3D('',#17604,#13679,#13680);
#10725=AXIS2_PLACEMENT_3D('',#17606,#13682,#13683);
#10726=AXIS2_PLACEMENT_3D('',#17608,#13684,#13685);
#10727=AXIS2_PLACEMENT_3D('',#17610,#13687,#13688);
#10728=AXIS2_PLACEMENT_3D('',#17612,#13689,#13690);
#10729=AXIS2_PLACEMENT_3D('',#17614,#13692,#13693);
#10730=AXIS2_PLACEMENT_3D('',#17616,#13694,#13695);
#10731=AXIS2_PLACEMENT_3D('',#17617,#13696,#13697);
#10732=AXIS2_PLACEMENT_3D('',#17619,#13698,#13699);
#10733=AXIS2_PLACEMENT_3D('',#17621,#13701,#13702);
#10734=AXIS2_PLACEMENT_3D('',#17623,#13703,#13704);
#10735=AXIS2_PLACEMENT_3D('',#17625,#13706,#13707);
#10736=AXIS2_PLACEMENT_3D('',#17627,#13708,#13709);
#10737=AXIS2_PLACEMENT_3D('',#17629,#13711,#13712);
#10738=AXIS2_PLACEMENT_3D('',#17630,#13713,#13714);
#10739=AXIS2_PLACEMENT_3D('',#17639,#13719,#13720);
#10740=AXIS2_PLACEMENT_3D('',#17645,#13724,#13725);
#10741=AXIS2_PLACEMENT_3D('',#17651,#13729,#13730);
#10742=AXIS2_PLACEMENT_3D('',#17657,#13734,#13735);
#10743=AXIS2_PLACEMENT_3D('',#17663,#13739,#13740);
#10744=AXIS2_PLACEMENT_3D('',#17666,#13743,#13744);
#10745=AXIS2_PLACEMENT_3D('',#17667,#13745,#13746);
#13671=DIRECTION('axis',(0.,0.,1.));
#13672=DIRECTION('refdir',(1.,0.,0.));
#13673=DIRECTION('center_axis',(0.,1.,0.));
#13674=DIRECTION('ref_axis',(0.,0.,1.));
#13675=DIRECTION('center_axis',(0.,-1.,0.));
#13676=DIRECTION('ref_axis',(1.,0.,0.));
#13677=DIRECTION('center_axis',(0.,-1.,0.));
#13678=DIRECTION('ref_axis',(1.,0.,0.));
#13679=DIRECTION('center_axis',(0.,-1.,0.));
#13680=DIRECTION('ref_axis',(1.,0.,0.));
#13681=DIRECTION('',(0.707106781186547,0.707106781186548,8.65956056235493E-17));
#13682=DIRECTION('center_axis',(0.,-1.,0.));
#13683=DIRECTION('ref_axis',(1.,0.,0.));
#13684=DIRECTION('center_axis',(0.,-1.,0.));
#13685=DIRECTION('ref_axis',(1.,0.,0.));
#13686=DIRECTION('',(0.,1.,0.));
#13687=DIRECTION('center_axis',(0.,1.,0.));
#13688=DIRECTION('ref_axis',(1.,0.,0.));
#13689=DIRECTION('center_axis',(0.,-1.,0.));
#13690=DIRECTION('ref_axis',(1.,0.,0.));
#13691=DIRECTION('',(-0.707106781186547,0.707106781186548,-8.65956056235493E-17));
#13692=DIRECTION('center_axis',(0.,-1.,0.));
#13693=DIRECTION('ref_axis',(0.,0.,-1.));
#13694=DIRECTION('center_axis',(0.,-1.,0.));
#13695=DIRECTION('ref_axis',(1.,0.,0.));
#13696=DIRECTION('center_axis',(0.,1.,0.));
#13697=DIRECTION('ref_axis',(1.,0.,0.));
#13698=DIRECTION('center_axis',(0.,1.,0.));
#13699=DIRECTION('ref_axis',(1.,0.,0.));
#13700=DIRECTION('',(-0.447213595499958,0.894427190999916,-5.47678698264203E-17));
#13701=DIRECTION('center_axis',(0.,-1.,0.));
#13702=DIRECTION('ref_axis',(1.,0.,0.));
#13703=DIRECTION('center_axis',(0.,1.,0.));
#13704=DIRECTION('ref_axis',(1.,0.,0.));
#13705=DIRECTION('',(0.,1.,0.));
#13706=DIRECTION('center_axis',(0.,1.,0.));
#13707=DIRECTION('ref_axis',(1.,0.,0.));
#13708=DIRECTION('center_axis',(0.,-1.,0.));
#13709=DIRECTION('ref_axis',(1.,0.,0.));
#13710=DIRECTION('',(-0.707106781186547,0.707106781186548,-8.65956056235493E-17));
#13711=DIRECTION('center_axis',(0.,-1.,0.));
#13712=DIRECTION('ref_axis',(0.,0.,-1.));
#13713=DIRECTION('center_axis',(0.866025403784439,0.,-0.5));
#13714=DIRECTION('ref_axis',(0.5,0.,0.866025403784439));
#13715=DIRECTION('',(-0.5,0.,-0.866025403784439));
#13716=DIRECTION('',(0.,-1.,0.));
#13717=DIRECTION('',(0.5,0.,0.866025403784439));
#13718=DIRECTION('',(0.,-1.,0.));
#13719=DIRECTION('center_axis',(1.60246890531964E-16,0.,-1.));
#13720=DIRECTION('ref_axis',(1.,0.,1.60246890531964E-16));
#13721=DIRECTION('',(-1.,0.,-1.60246890531964E-16));
#13722=DIRECTION('',(0.,-1.,0.));
#13723=DIRECTION('',(1.,0.,1.60246890531964E-16));
#13724=DIRECTION('center_axis',(-0.866025403784439,0.,-0.5));
#13725=DIRECTION('ref_axis',(0.5,0.,-0.866025403784439));
#13726=DIRECTION('',(-0.5,0.,0.866025403784439));
#13727=DIRECTION('',(0.,-1.,0.));
#13728=DIRECTION('',(0.5,0.,-0.866025403784439));
#13729=DIRECTION('center_axis',(-0.866025403784439,0.,0.5));
#13730=DIRECTION('ref_axis',(-0.5,0.,-0.866025403784439));
#13731=DIRECTION('',(0.5,0.,0.866025403784439));
#13732=DIRECTION('',(0.,-1.,0.));
#13733=DIRECTION('',(-0.5,0.,-0.866025403784439));
#13734=DIRECTION('center_axis',(-1.60246890531964E-16,0.,1.));
#13735=DIRECTION('ref_axis',(-1.,0.,-1.60246890531964E-16));
#13736=DIRECTION('',(1.,0.,1.60246890531964E-16));
#13737=DIRECTION('',(0.,-1.,0.));
#13738=DIRECTION('',(-1.,0.,-1.60246890531964E-16));
#13739=DIRECTION('center_axis',(0.866025403784439,0.,0.5));
#13740=DIRECTION('ref_axis',(-0.5,0.,0.866025403784439));
#13741=DIRECTION('',(0.5,0.,-0.866025403784439));
#13742=DIRECTION('',(-0.5,0.,0.866025403784439));
#13743=DIRECTION('center_axis',(0.,1.,0.));
#13744=DIRECTION('ref_axis',(1.,0.,0.));
#13745=DIRECTION('center_axis',(0.,-1.,0.));
#13746=DIRECTION('ref_axis',(0.,0.,-1.));
#17598=CARTESIAN_POINT('',(0.,0.,0.));
#17599=CARTESIAN_POINT('Origin',(0.3,0.4,0.));
#17600=CARTESIAN_POINT('',(-0.3,0.4,-3.67394039744206E-17));
#17601=CARTESIAN_POINT('Origin',(0.,0.4,0.));
#17602=CARTESIAN_POINT('Origin',(0.,0.375,0.));
#17603=CARTESIAN_POINT('',(-0.35,0.35,-4.28626379701573E-17));
#17604=CARTESIAN_POINT('Origin',(0.,0.35,0.));
#17605=CARTESIAN_POINT('',(-0.325,0.375,-3.9801020972289E-17));
#17606=CARTESIAN_POINT('Origin',(0.,0.19,0.));
#17607=CARTESIAN_POINT('',(-0.35,0.03,-4.28626379701574E-17));
#17608=CARTESIAN_POINT('Origin',(0.,0.03,0.));
#17609=CARTESIAN_POINT('',(-0.35,0.19,-4.28626379701574E-17));
#17610=CARTESIAN_POINT('Origin',(0.,0.0149999999999999,0.));
#17611=CARTESIAN_POINT('',(-0.32,-3.29597460435593E-17,-3.91886975727153E-17));
#17612=CARTESIAN_POINT('Origin',(0.,0.,0.));
#17613=CARTESIAN_POINT('',(-0.335,0.0149999999999999,-4.10256677714363E-17));
#17614=CARTESIAN_POINT('Origin',(0.22,0.,0.));
#17615=CARTESIAN_POINT('',(-0.22,-6.93889390390723E-18,-2.69422295812418E-17));
#17616=CARTESIAN_POINT('Origin',(0.,0.,0.));
#17617=CARTESIAN_POINT('Origin',(0.,-0.02,0.));
#17618=CARTESIAN_POINT('',(-0.1954,-0.0492,2.39295984553393E-17));
#17619=CARTESIAN_POINT('Origin',(0.,-0.0492,0.));
#17620=CARTESIAN_POINT('',(-0.21,-0.02,-2.57175827820944E-17));
#17621=CARTESIAN_POINT('Origin',(0.,-0.8,0.));
#17622=CARTESIAN_POINT('',(-0.1954,-1.5646,2.39295984553393E-17));
#17623=CARTESIAN_POINT('Origin',(0.,-1.5646,0.));
#17624=CARTESIAN_POINT('',(-0.1954,-0.8,-2.39295984553393E-17));
#17625=CARTESIAN_POINT('Origin',(0.,-1.58,0.));
#17626=CARTESIAN_POINT('',(-0.16,-1.6,-1.95943487863577E-17));
#17627=CARTESIAN_POINT('Origin',(0.,-1.6,0.));
#17628=CARTESIAN_POINT('',(-0.18,-1.58,-2.20436423846524E-17));
#17629=CARTESIAN_POINT('Origin',(0.,-1.6,0.));
#17630=CARTESIAN_POINT('Origin',(0.0866025403784439,-0.4,-0.15));
#17631=CARTESIAN_POINT('',(0.173205080756888,-0.4,0.));
#17632=CARTESIAN_POINT('',(0.0866025403784439,-0.4,-0.15));
#17633=CARTESIAN_POINT('',(0.173205080756888,-0.4,0.));
#17634=CARTESIAN_POINT('',(0.0866025403784439,-0.64,-0.15));
#17635=CARTESIAN_POINT('',(0.0866025403784439,-0.4,-0.15));
#17636=CARTESIAN_POINT('',(0.173205080756888,-0.64,0.));
#17637=CARTESIAN_POINT('',(0.173205080756888,-0.64,0.));
#17638=CARTESIAN_POINT('',(0.173205080756888,-0.4,0.));
#17639=CARTESIAN_POINT('Origin',(-0.0866025403784438,-0.4,-0.15));
#17640=CARTESIAN_POINT('',(-0.0866025403784438,-0.4,-0.15));
#17641=CARTESIAN_POINT('',(0.0866025403784439,-0.4,-0.15));
#17642=CARTESIAN_POINT('',(-0.0866025403784438,-0.64,-0.15));
#17643=CARTESIAN_POINT('',(-0.0866025403784438,-0.4,-0.15));
#17644=CARTESIAN_POINT('',(0.0866025403784439,-0.64,-0.15));
#17645=CARTESIAN_POINT('Origin',(-0.173205080756888,-0.4,-2.77555756156289E-17));
#17646=CARTESIAN_POINT('',(-0.173205080756888,-0.4,-2.12115047744981E-17));
#17647=CARTESIAN_POINT('',(-0.0866025403784438,-0.4,-0.15));
#17648=CARTESIAN_POINT('',(-0.173205080756888,-0.64,-2.77555756156289E-17));
#17649=CARTESIAN_POINT('',(-0.173205080756888,-0.4,-2.12115047744981E-17));
#17650=CARTESIAN_POINT('',(-0.0866025403784438,-0.64,-0.15));
#17651=CARTESIAN_POINT('Origin',(-0.0866025403784439,-0.4,0.15));
#17652=CARTESIAN_POINT('',(-0.0866025403784439,-0.4,0.15));
#17653=CARTESIAN_POINT('',(-0.173205080756888,-0.4,-2.12115047744981E-17));
#17654=CARTESIAN_POINT('',(-0.0866025403784439,-0.64,0.15));
#17655=CARTESIAN_POINT('',(-0.0866025403784439,-0.4,0.15));
#17656=CARTESIAN_POINT('',(-0.173205080756888,-0.64,-2.12115047744981E-17));
#17657=CARTESIAN_POINT('Origin',(0.0866025403784439,-0.4,0.15));
#17658=CARTESIAN_POINT('',(0.0866025403784439,-0.4,0.15));
#17659=CARTESIAN_POINT('',(-0.0866025403784439,-0.4,0.15));
#17660=CARTESIAN_POINT('',(0.0866025403784439,-0.64,0.15));
#17661=CARTESIAN_POINT('',(0.0866025403784439,-0.4,0.15));
#17662=CARTESIAN_POINT('',(-0.0866025403784439,-0.64,0.15));
#17663=CARTESIAN_POINT('Origin',(0.173205080756888,-0.4,0.));
#17664=CARTESIAN_POINT('',(0.0866025403784439,-0.4,0.15));
#17665=CARTESIAN_POINT('',(0.0866025403784439,-0.64,0.15));
#17666=CARTESIAN_POINT('Origin',(0.,-0.4,-2.77555756156289E-17));
#17667=CARTESIAN_POINT('Origin',(0.,-0.64,-2.77555756156289E-17));
#17779=UNCERTAINTY_MEASURE_WITH_UNIT(LENGTH_MEASURE(0.001),#17831,
'DISTANCE_ACCURACY_VALUE',
'Maximum model space distance between geometric entities at asserted c
onnectivities');
#17780=UNCERTAINTY_MEASURE_WITH_UNIT(LENGTH_MEASURE(0.001),#17831,
'DISTANCE_ACCURACY_VALUE',
'Maximum model space distance between geometric entities at asserted c
onnectivities');
#17829=(
GEOMETRIC_REPRESENTATION_CONTEXT(3)
GLOBAL_UNCERTAINTY_ASSIGNED_CONTEXT((#17779))
GLOBAL_UNIT_ASSIGNED_CONTEXT((#17831,#17833,#17834))
REPRESENTATION_CONTEXT('','3D')
);
#17830=(
GEOMETRIC_REPRESENTATION_CONTEXT(3)
GLOBAL_UNCERTAINTY_ASSIGNED_CONTEXT((#17780))
GLOBAL_UNIT_ASSIGNED_CONTEXT((#17831,#17833,#17834))
REPRESENTATION_CONTEXT('','3D')
);
#17831=(
LENGTH_UNIT()
NAMED_UNIT(*)
SI_UNIT(.CENTI.,.METRE.)
);
#17833=(
NAMED_UNIT(*)
PLANE_ANGLE_UNIT()
SI_UNIT($,.RADIAN.)
);
#17834=(
NAMED_UNIT(*)
SI_UNIT($,.STERADIAN.)
SOLID_ANGLE_UNIT()
);
#17883=SHAPE_DEFINITION_REPRESENTATION(#17942,#18054);
#17942=PRODUCT_DEFINITION_SHAPE('',$,#18104);
#18054=SHAPE_REPRESENTATION('',(#10720),#17829);
#18055=PRODUCT_DEFINITION_CONTEXT('part definition',#18204,'design');
#18104=PRODUCT_DEFINITION('Cap Screw - M4x16','Cap Screw - M4x16',#18153,
#18055);
#18153=PRODUCT_DEFINITION_FORMATION('',$,#18254);
#18204=APPLICATION_CONTEXT(
'Core Data for Automotive Mechanical Design Process');
#18205=PRODUCT_CONTEXT('part definition',#18204,'mechanical');
#18254=PRODUCT('Cap Screw - M4x16','Cap Screw - M4x16',
'Cap Screw - M4x16',(#18205));
#18318=COLOUR_RGB('Black',0.12,0.14,0.17);
#18319=FILL_AREA_STYLE_COLOUR('',#18318);
#18320=FILL_AREA_STYLE('',(#18319));
#18321=SURFACE_STYLE_FILL_AREA(#18320);
#18322=SURFACE_SIDE_STYLE('',(#18321));
#18323=SURFACE_STYLE_USAGE(.BOTH.,#18322);
#18324=PRESENTATION_STYLE_ASSIGNMENT((#18323));
ENDSEC;
END-ISO-10303-21;
